ISO-10303-21;
HEADER;
/* Generated by software containing ST-Developer
 * from STEP Tools, Inc. (www.steptools.com) 
 */

FILE_DESCRIPTION(
/* description */ ('Self-centering screw clamp'),
/* implementation_level */ '2;1');

FILE_NAME(
/* name */ 'Right screw nut.step',
/* time_stamp */ '2026-10-28T03:25:31-07:00',
/* author */ (''),
/* organization */ (''),
/* preprocessor_version */ 'ST-DEVELOPER v20.2',
/* originating_system */ 'Autodesk Translation Framework v15.17.0.0',
/* authorisation */ '');

FILE_SCHEMA (('AUTOMOTIVE_DESIGN { 1 0 10303 214 3 1 1 }'));
ENDSEC;

DATA;
#10=MECHANICAL_DESIGN_GEOMETRIC_PRESENTATION_REPRESENTATION('',(#658),#16799);
#569=SHAPE_REPRESENTATION_RELATIONSHIP('SRR','None',#17045,#610);
#610=ADVANCED_BREP_SHAPE_REPRESENTATION('',(#706),#16783);
#658=STYLED_ITEM('',(#17333),#706);
#706=MANIFOLD_SOLID_BREP('Body1',#9109);
#964=FACE_BOUND('',#2388,.T.);
#965=FACE_BOUND('',#2391,.T.);
#966=FACE_BOUND('',#2392,.T.);
#967=FACE_BOUND('',#2393,.T.);
#968=FACE_BOUND('',#2396,.T.);
#1185=PLANE('',#10365);
#1186=PLANE('',#10372);
#1187=PLANE('',#10384);
#1188=PLANE('',#10388);
#1189=PLANE('',#10392);
#1632=FACE_OUTER_BOUND('',#2382,.T.);
#1633=FACE_OUTER_BOUND('',#2383,.T.);
#1634=FACE_OUTER_BOUND('',#2384,.T.);
#1635=FACE_OUTER_BOUND('',#2385,.T.);
#1636=FACE_OUTER_BOUND('',#2386,.T.);
#1637=FACE_OUTER_BOUND('',#2387,.T.);
#1638=FACE_OUTER_BOUND('',#2389,.T.);
#1639=FACE_OUTER_BOUND('',#2390,.T.);
#1640=FACE_OUTER_BOUND('',#2394,.T.);
#1641=FACE_OUTER_BOUND('',#2395,.T.);
#2382=EDGE_LOOP('',(#7785,#7786,#7787));
#2383=EDGE_LOOP('',(#7788,#7789,#7790,#7791,#7792,#7793,#7794,#7795));
#2384=EDGE_LOOP('',(#7796,#7797,#7798));
#2385=EDGE_LOOP('',(#7799,#7800,#7801,#7802,#7803,#7804,#7805,#7806));
#2386=EDGE_LOOP('',(#7807,#7808,#7809,#7810,#7811,#7812,#7813,#7814,#7815,
#7816,#7817,#7818));
#2387=EDGE_LOOP('',(#7819));
#2388=EDGE_LOOP('',(#7820,#7821,#7822,#7823,#7824));
#2389=EDGE_LOOP('',(#7825,#7826,#7827,#7828));
#2390=EDGE_LOOP('',(#7829));
#2391=EDGE_LOOP('',(#7830));
#2392=EDGE_LOOP('',(#7831));
#2393=EDGE_LOOP('',(#7832));
#2394=EDGE_LOOP('',(#7833,#7834,#7835,#7836));
#2395=EDGE_LOOP('',(#7837));
#2396=EDGE_LOOP('',(#7838));
#2997=LINE('',#15853,#3570);
#2998=LINE('',#15855,#3571);
#2999=LINE('',#15858,#3572);
#3000=LINE('',#15870,#3573);
#3001=LINE('',#15873,#3574);
#3002=LINE('',#15875,#3575);
#3003=LINE('',#15880,#3576);
#3004=LINE('',#15888,#3577);
#3005=LINE('',#15896,#3578);
#3570=VECTOR('',#12760,0.225);
#3571=VECTOR('',#12761,1.);
#3572=VECTOR('',#12764,1.);
#3573=VECTOR('',#12777,0.225);
#3574=VECTOR('',#12780,1.);
#3575=VECTOR('',#12781,1.);
#3576=VECTOR('',#12788,1.1);
#3577=VECTOR('',#12799,1.6);
#3578=VECTOR('',#12810,0.525);
#4114=CIRCLE('',#10366,1.1);
#4115=CIRCLE('',#10367,0.225);
#4116=CIRCLE('',#10368,0.225);
#4117=CIRCLE('',#10370,0.225);
#4118=CIRCLE('',#10371,0.225);
#4119=CIRCLE('',#10373,1.1);
#4120=CIRCLE('',#10374,0.225);
#4121=CIRCLE('',#10375,1.1);
#4122=CIRCLE('',#10377,0.225);
#4123=CIRCLE('',#10378,0.225);
#4124=CIRCLE('',#10379,0.225);
#4125=CIRCLE('',#10381,1.1);
#4126=CIRCLE('',#10382,1.1);
#4127=CIRCLE('',#10383,1.1);
#4128=CIRCLE('',#10385,1.6);
#4129=CIRCLE('',#10387,1.6);
#4130=CIRCLE('',#10389,0.525);
#4131=CIRCLE('',#10391,0.525);
#4789=VERTEX_POINT('',#15844);
#4790=VERTEX_POINT('',#15845);
#4791=VERTEX_POINT('',#15847);
#4792=VERTEX_POINT('',#15851);
#4793=VERTEX_POINT('',#15854);
#4794=VERTEX_POINT('',#15856);
#4795=VERTEX_POINT('',#15860);
#4796=VERTEX_POINT('',#15861);
#4797=VERTEX_POINT('',#15863);
#4798=VERTEX_POINT('',#15867);
#4799=VERTEX_POINT('',#15869);
#4800=VERTEX_POINT('',#15871);
#4801=VERTEX_POINT('',#15874);
#4802=VERTEX_POINT('',#15878);
#4803=VERTEX_POINT('',#15884);
#4804=VERTEX_POINT('',#15887);
#4805=VERTEX_POINT('',#15891);
#4806=VERTEX_POINT('',#15894);
#5817=EDGE_CURVE('',#4789,#4790,#4114,.T.);
#5818=EDGE_CURVE('',#4791,#4789,#4115,.T.);
#5819=EDGE_CURVE('',#4790,#4791,#4116,.T.);
#5820=EDGE_CURVE('',#4792,#4792,#4117,.T.);
#5821=EDGE_CURVE('',#4792,#4791,#2997,.T.);
#5822=EDGE_CURVE('',#4793,#4789,#2998,.T.);
#5823=EDGE_CURVE('',#4794,#4793,#4118,.T.);
#5824=EDGE_CURVE('',#4790,#4794,#2999,.T.);
#5825=EDGE_CURVE('',#4795,#4796,#4119,.T.);
#5826=EDGE_CURVE('',#4797,#4795,#4120,.T.);
#5827=EDGE_CURVE('',#4796,#4797,#4121,.T.);
#5828=EDGE_CURVE('',#4798,#4798,#4122,.T.);
#5829=EDGE_CURVE('',#4798,#4799,#3000,.T.);
#5830=EDGE_CURVE('',#4800,#4799,#4123,.T.);
#5831=EDGE_CURVE('',#4797,#4800,#3001,.T.);
#5832=EDGE_CURVE('',#4801,#4795,#3002,.T.);
#5833=EDGE_CURVE('',#4799,#4801,#4124,.T.);
#5834=EDGE_CURVE('',#4802,#4802,#4125,.T.);
#5835=EDGE_CURVE('',#4802,#4796,#3003,.T.);
#5836=EDGE_CURVE('',#4800,#4793,#4126,.T.);
#5837=EDGE_CURVE('',#4794,#4801,#4127,.T.);
#5838=EDGE_CURVE('',#4803,#4803,#4128,.T.);
#5839=EDGE_CURVE('',#4803,#4804,#3004,.T.);
#5840=EDGE_CURVE('',#4804,#4804,#4129,.T.);
#5841=EDGE_CURVE('',#4805,#4805,#4130,.T.);
#5842=EDGE_CURVE('',#4806,#4806,#4131,.T.);
#5843=EDGE_CURVE('',#4806,#4805,#3005,.T.);
#7785=ORIENTED_EDGE('',*,*,#5817,.F.);
#7786=ORIENTED_EDGE('',*,*,#5818,.F.);
#7787=ORIENTED_EDGE('',*,*,#5819,.F.);
#7788=ORIENTED_EDGE('',*,*,#5820,.F.);
#7789=ORIENTED_EDGE('',*,*,#5821,.T.);
#7790=ORIENTED_EDGE('',*,*,#5818,.T.);
#7791=ORIENTED_EDGE('',*,*,#5822,.F.);
#7792=ORIENTED_EDGE('',*,*,#5823,.F.);
#7793=ORIENTED_EDGE('',*,*,#5824,.F.);
#7794=ORIENTED_EDGE('',*,*,#5819,.T.);
#7795=ORIENTED_EDGE('',*,*,#5821,.F.);
#7796=ORIENTED_EDGE('',*,*,#5825,.F.);
#7797=ORIENTED_EDGE('',*,*,#5826,.F.);
#7798=ORIENTED_EDGE('',*,*,#5827,.F.);
#7799=ORIENTED_EDGE('',*,*,#5828,.F.);
#7800=ORIENTED_EDGE('',*,*,#5829,.T.);
#7801=ORIENTED_EDGE('',*,*,#5830,.F.);
#7802=ORIENTED_EDGE('',*,*,#5831,.F.);
#7803=ORIENTED_EDGE('',*,*,#5826,.T.);
#7804=ORIENTED_EDGE('',*,*,#5832,.F.);
#7805=ORIENTED_EDGE('',*,*,#5833,.F.);
#7806=ORIENTED_EDGE('',*,*,#5829,.F.);
#7807=ORIENTED_EDGE('',*,*,#5834,.F.);
#7808=ORIENTED_EDGE('',*,*,#5835,.T.);
#7809=ORIENTED_EDGE('',*,*,#5827,.T.);
#7810=ORIENTED_EDGE('',*,*,#5831,.T.);
#7811=ORIENTED_EDGE('',*,*,#5836,.T.);
#7812=ORIENTED_EDGE('',*,*,#5822,.T.);
#7813=ORIENTED_EDGE('',*,*,#5817,.T.);
#7814=ORIENTED_EDGE('',*,*,#5824,.T.);
#7815=ORIENTED_EDGE('',*,*,#5837,.T.);
#7816=ORIENTED_EDGE('',*,*,#5832,.T.);
#7817=ORIENTED_EDGE('',*,*,#5825,.T.);
#7818=ORIENTED_EDGE('',*,*,#5835,.F.);
#7819=ORIENTED_EDGE('',*,*,#5838,.T.);
#7820=ORIENTED_EDGE('',*,*,#5823,.T.);
#7821=ORIENTED_EDGE('',*,*,#5836,.F.);
#7822=ORIENTED_EDGE('',*,*,#5830,.T.);
#7823=ORIENTED_EDGE('',*,*,#5833,.T.);
#7824=ORIENTED_EDGE('',*,*,#5837,.F.);
#7825=ORIENTED_EDGE('',*,*,#5838,.F.);
#7826=ORIENTED_EDGE('',*,*,#5839,.T.);
#7827=ORIENTED_EDGE('',*,*,#5840,.T.);
#7828=ORIENTED_EDGE('',*,*,#5839,.F.);
#7829=ORIENTED_EDGE('',*,*,#5840,.F.);
#7830=ORIENTED_EDGE('',*,*,#5820,.T.);
#7831=ORIENTED_EDGE('',*,*,#5828,.T.);
#7832=ORIENTED_EDGE('',*,*,#5841,.F.);
#7833=ORIENTED_EDGE('',*,*,#5842,.F.);
#7834=ORIENTED_EDGE('',*,*,#5843,.T.);
#7835=ORIENTED_EDGE('',*,*,#5841,.T.);
#7836=ORIENTED_EDGE('',*,*,#5843,.F.);
#7837=ORIENTED_EDGE('',*,*,#5834,.T.);
#7838=ORIENTED_EDGE('',*,*,#5842,.T.);
#8523=CYLINDRICAL_SURFACE('',#10369,0.225);
#8524=CYLINDRICAL_SURFACE('',#10376,0.225);
#8525=CYLINDRICAL_SURFACE('',#10380,1.1);
#8526=CYLINDRICAL_SURFACE('',#10386,1.6);
#8527=CYLINDRICAL_SURFACE('',#10390,0.525);
#8930=ADVANCED_FACE('',(#1632),#1185,.F.);
#8931=ADVANCED_FACE('',(#1633),#8523,.F.);
#8932=ADVANCED_FACE('',(#1634),#1186,.F.);
#8933=ADVANCED_FACE('',(#1635),#8524,.F.);
#8934=ADVANCED_FACE('',(#1636),#8525,.T.);
#8935=ADVANCED_FACE('',(#1637,#964),#1187,.T.);
#8936=ADVANCED_FACE('',(#1638),#8526,.T.);
#8937=ADVANCED_FACE('',(#1639,#965,#966,#967),#1188,.F.);
#8938=ADVANCED_FACE('',(#1640),#8527,.F.);
#8939=ADVANCED_FACE('',(#1641,#968),#1189,.T.);
#9109=CLOSED_SHELL('',(#8930,#8931,#8932,#8933,#8934,#8935,#8936,#8937,
#8938,#8939));
#10364=AXIS2_PLACEMENT_3D('',#15842,#12746,#12747);
#10365=AXIS2_PLACEMENT_3D('',#15843,#12748,#12749);
#10366=AXIS2_PLACEMENT_3D('',#15846,#12750,#12751);
#10367=AXIS2_PLACEMENT_3D('',#15848,#12752,#12753);
#10368=AXIS2_PLACEMENT_3D('',#15849,#12754,#12755);
#10369=AXIS2_PLACEMENT_3D('',#15850,#12756,#12757);
#10370=AXIS2_PLACEMENT_3D('',#15852,#12758,#12759);
#10371=AXIS2_PLACEMENT_3D('',#15857,#12762,#12763);
#10372=AXIS2_PLACEMENT_3D('',#15859,#12765,#12766);
#10373=AXIS2_PLACEMENT_3D('',#15862,#12767,#12768);
#10374=AXIS2_PLACEMENT_3D('',#15864,#12769,#12770);
#10375=AXIS2_PLACEMENT_3D('',#15865,#12771,#12772);
#10376=AXIS2_PLACEMENT_3D('',#15866,#12773,#12774);
#10377=AXIS2_PLACEMENT_3D('',#15868,#12775,#12776);
#10378=AXIS2_PLACEMENT_3D('',#15872,#12778,#12779);
#10379=AXIS2_PLACEMENT_3D('',#15876,#12782,#12783);
#10380=AXIS2_PLACEMENT_3D('',#15877,#12784,#12785);
#10381=AXIS2_PLACEMENT_3D('',#15879,#12786,#12787);
#10382=AXIS2_PLACEMENT_3D('',#15881,#12789,#12790);
#10383=AXIS2_PLACEMENT_3D('',#15882,#12791,#12792);
#10384=AXIS2_PLACEMENT_3D('',#15883,#12793,#12794);
#10385=AXIS2_PLACEMENT_3D('',#15885,#12795,#12796);
#10386=AXIS2_PLACEMENT_3D('',#15886,#12797,#12798);
#10387=AXIS2_PLACEMENT_3D('',#15889,#12800,#12801);
#10388=AXIS2_PLACEMENT_3D('',#15890,#12802,#12803);
#10389=AXIS2_PLACEMENT_3D('',#15892,#12804,#12805);
#10390=AXIS2_PLACEMENT_3D('',#15893,#12806,#12807);
#10391=AXIS2_PLACEMENT_3D('',#15895,#12808,#12809);
#10392=AXIS2_PLACEMENT_3D('',#15897,#12811,#12812);
#12746=DIRECTION('axis',(0.,0.,1.));
#12747=DIRECTION('refdir',(1.,0.,0.));
#12748=DIRECTION('center_axis',(1.,0.,0.));
#12749=DIRECTION('ref_axis',(0.,0.,-1.));
#12750=DIRECTION('center_axis',(1.,0.,0.));
#12751=DIRECTION('ref_axis',(0.,0.,-1.));
#12752=DIRECTION('center_axis',(1.,0.,0.));
#12753=DIRECTION('ref_axis',(0.,0.,-1.));
#12754=DIRECTION('center_axis',(1.,0.,0.));
#12755=DIRECTION('ref_axis',(0.,0.,-1.));
#12756=DIRECTION('center_axis',(1.,0.,0.));
#12757=DIRECTION('ref_axis',(0.,0.,-1.));
#12758=DIRECTION('center_axis',(1.,0.,0.));
#12759=DIRECTION('ref_axis',(0.,0.,-1.));
#12760=DIRECTION('',(1.,0.,0.));
#12761=DIRECTION('',(1.,0.,0.));
#12762=DIRECTION('center_axis',(-1.,0.,0.));
#12763=DIRECTION('ref_axis',(0.,0.,-1.));
#12764=DIRECTION('',(-1.,0.,0.));
#12765=DIRECTION('center_axis',(1.,0.,0.));
#12766=DIRECTION('ref_axis',(0.,0.,-1.));
#12767=DIRECTION('center_axis',(1.,0.,0.));
#12768=DIRECTION('ref_axis',(0.,0.,-1.));
#12769=DIRECTION('center_axis',(1.,0.,0.));
#12770=DIRECTION('ref_axis',(0.,0.,-1.));
#12771=DIRECTION('center_axis',(1.,0.,0.));
#12772=DIRECTION('ref_axis',(0.,0.,-1.));
#12773=DIRECTION('center_axis',(1.,0.,0.));
#12774=DIRECTION('ref_axis',(0.,0.,-1.));
#12775=DIRECTION('center_axis',(1.,0.,0.));
#12776=DIRECTION('ref_axis',(0.,0.,-1.));
#12777=DIRECTION('',(1.,0.,0.));
#12778=DIRECTION('center_axis',(-1.,0.,0.));
#12779=DIRECTION('ref_axis',(0.,0.,-1.));
#12780=DIRECTION('',(-1.,0.,0.));
#12781=DIRECTION('',(1.,0.,0.));
#12782=DIRECTION('center_axis',(-1.,0.,0.));
#12783=DIRECTION('ref_axis',(0.,0.,-1.));
#12784=DIRECTION('center_axis',(1.,0.,0.));
#12785=DIRECTION('ref_axis',(0.,0.,-1.));
#12786=DIRECTION('center_axis',(1.,0.,0.));
#12787=DIRECTION('ref_axis',(0.,0.,-1.));
#12788=DIRECTION('',(-1.,0.,0.));
#12789=DIRECTION('center_axis',(1.,0.,0.));
#12790=DIRECTION('ref_axis',(0.,0.,-1.));
#12791=DIRECTION('center_axis',(1.,0.,0.));
#12792=DIRECTION('ref_axis',(0.,0.,-1.));
#12793=DIRECTION('center_axis',(1.,0.,0.));
#12794=DIRECTION('ref_axis',(0.,0.,-1.));
#12795=DIRECTION('center_axis',(1.,0.,0.));
#12796=DIRECTION('ref_axis',(0.,0.,-1.));
#12797=DIRECTION('center_axis',(1.,0.,0.));
#12798=DIRECTION('ref_axis',(0.,0.,-1.));
#12799=DIRECTION('',(-1.,0.,0.));
#12800=DIRECTION('center_axis',(1.,0.,0.));
#12801=DIRECTION('ref_axis',(0.,0.,-1.));
#12802=DIRECTION('center_axis',(1.,0.,0.));
#12803=DIRECTION('ref_axis',(0.,0.,-1.));
#12804=DIRECTION('center_axis',(-1.,0.,0.));
#12805=DIRECTION('ref_axis',(0.,0.,-1.));
#12806=DIRECTION('center_axis',(1.,0.,0.));
#12807=DIRECTION('ref_axis',(0.,0.,-1.));
#12808=DIRECTION('center_axis',(-1.,0.,0.));
#12809=DIRECTION('ref_axis',(0.,0.,-1.));
#12810=DIRECTION('',(-1.,0.,0.));
#12811=DIRECTION('center_axis',(1.,0.,0.));
#12812=DIRECTION('ref_axis',(0.,0.,-1.));
#15842=CARTESIAN_POINT('',(0.,0.,0.));
#15843=CARTESIAN_POINT('Origin',(5.6,0.,2.7));
#15844=CARTESIAN_POINT('',(5.6,-0.0947295350922144,2.90408653846154));
#15845=CARTESIAN_POINT('',(5.6,0.0947295350922144,2.90408653846154));
#15846=CARTESIAN_POINT('Origin',(5.6,0.,4.));
#15847=CARTESIAN_POINT('',(5.6,-2.75545529808155E-17,2.925));
#15848=CARTESIAN_POINT('Origin',(5.6,0.,2.7));
#15849=CARTESIAN_POINT('Origin',(5.6,0.,2.7));
#15850=CARTESIAN_POINT('Origin',(5.,0.,2.7));
#15851=CARTESIAN_POINT('',(5.1,-2.75545529808155E-17,2.925));
#15852=CARTESIAN_POINT('Origin',(5.1,0.,2.7));
#15853=CARTESIAN_POINT('',(5.,-2.75545529808155E-17,2.925));
#15854=CARTESIAN_POINT('',(5.5,-0.0947295350922147,2.90408653846154));
#15855=CARTESIAN_POINT('',(5.,-0.0947295350922144,2.90408653846154));
#15856=CARTESIAN_POINT('',(5.5,0.0947295350922147,2.90408653846154));
#15857=CARTESIAN_POINT('Origin',(5.5,0.,2.7));
#15858=CARTESIAN_POINT('',(5.,0.0947295350922144,2.90408653846154));
#15859=CARTESIAN_POINT('Origin',(5.6,0.,5.3));
#15860=CARTESIAN_POINT('',(5.6,0.0947295350922135,5.09591346153846));
#15861=CARTESIAN_POINT('',(5.6,-1.34711147906209E-16,5.1));
#15862=CARTESIAN_POINT('Origin',(5.6,0.,4.));
#15863=CARTESIAN_POINT('',(5.6,-0.0947295350922135,5.09591346153846));
#15864=CARTESIAN_POINT('Origin',(5.6,0.,5.3));
#15865=CARTESIAN_POINT('Origin',(5.6,0.,4.));
#15866=CARTESIAN_POINT('Origin',(5.,0.,5.3));
#15867=CARTESIAN_POINT('',(5.1,-2.75545529808154E-17,5.525));
#15868=CARTESIAN_POINT('Origin',(5.1,0.,5.3));
#15869=CARTESIAN_POINT('',(5.5,-2.75545529808154E-17,5.525));
#15870=CARTESIAN_POINT('',(5.,-2.75545529808154E-17,5.525));
#15871=CARTESIAN_POINT('',(5.5,-0.0947295350922147,5.09591346153846));
#15872=CARTESIAN_POINT('Origin',(5.5,0.,5.3));
#15873=CARTESIAN_POINT('',(5.,-0.0947295350922135,5.09591346153846));
#15874=CARTESIAN_POINT('',(5.5,0.0947295350922147,5.09591346153846));
#15875=CARTESIAN_POINT('',(5.,0.0947295350922135,5.09591346153846));
#15876=CARTESIAN_POINT('Origin',(5.5,0.,5.3));
#15877=CARTESIAN_POINT('Origin',(5.5,0.,4.));
#15878=CARTESIAN_POINT('',(8.5,-1.34711147906209E-16,5.1));
#15879=CARTESIAN_POINT('Origin',(8.5,0.,4.));
#15880=CARTESIAN_POINT('',(5.5,-1.34711147906209E-16,5.1));
#15881=CARTESIAN_POINT('Origin',(5.5,0.,4.));
#15882=CARTESIAN_POINT('Origin',(5.5,0.,4.));
#15883=CARTESIAN_POINT('Origin',(5.5,0.,4.));
#15884=CARTESIAN_POINT('',(5.5,-1.95943487863577E-16,5.6));
#15885=CARTESIAN_POINT('Origin',(5.5,0.,4.));
#15886=CARTESIAN_POINT('Origin',(5.1,0.,4.));
#15887=CARTESIAN_POINT('',(5.1,-1.95943487863577E-16,5.6));
#15888=CARTESIAN_POINT('',(5.1,-1.95943487863577E-16,5.6));
#15889=CARTESIAN_POINT('Origin',(5.1,0.,4.));
#15890=CARTESIAN_POINT('Origin',(5.1,0.,4.));
#15891=CARTESIAN_POINT('',(5.1,-6.4293956955236E-17,4.525));
#15892=CARTESIAN_POINT('Origin',(5.1,0.,4.));
#15893=CARTESIAN_POINT('Origin',(5.5,0.,4.));
#15894=CARTESIAN_POINT('',(8.5,-6.4293956955236E-17,4.525));
#15895=CARTESIAN_POINT('Origin',(8.5,0.,4.));
#15896=CARTESIAN_POINT('',(5.5,-6.4293956955236E-17,4.525));
#15897=CARTESIAN_POINT('Origin',(8.5,0.,4.));
#16734=UNCERTAINTY_MEASURE_WITH_UNIT(LENGTH_MEASURE(0.001),#16800,
'DISTANCE_ACCURACY_VALUE',
'Maximum model space distance between geometric entities at asserted c
onnectivities');
#16750=UNCERTAINTY_MEASURE_WITH_UNIT(LENGTH_MEASURE(0.001),#16800,
'DISTANCE_ACCURACY_VALUE',
'Maximum model space distance between geometric entities at asserted c
onnectivities');
#16783=(
GEOMETRIC_REPRESENTATION_CONTEXT(3)
GLOBAL_UNCERTAINTY_ASSIGNED_CONTEXT((#16734))
GLOBAL_UNIT_ASSIGNED_CONTEXT((#16800,#16802,#16803))
REPRESENTATION_CONTEXT('','3D')
);
#16799=(
GEOMETRIC_REPRESENTATION_CONTEXT(3)
GLOBAL_UNCERTAINTY_ASSIGNED_CONTEXT((#16750))
GLOBAL_UNIT_ASSIGNED_CONTEXT((#16800,#16802,#16803))
REPRESENTATION_CONTEXT('','3D')
);
#16800=(
LENGTH_UNIT()
NAMED_UNIT(*)
SI_UNIT(.CENTI.,.METRE.)
);
#16802=(
NAMED_UNIT(*)
PLANE_ANGLE_UNIT()
SI_UNIT($,.RADIAN.)
);
#16803=(
NAMED_UNIT(*)
SI_UNIT($,.STERADIAN.)
SOLID_ANGLE_UNIT()
);
#16836=SHAPE_DEFINITION_REPRESENTATION(#16889,#17045);
#16889=PRODUCT_DEFINITION_SHAPE('',$,#17094);
#17045=SHAPE_REPRESENTATION('',(#10364),#16783);
#17061=PRODUCT_DEFINITION_CONTEXT('part definition',#17207,'design');
#17094=PRODUCT_DEFINITION('Right screw nut','Right screw nut',#17142,#17061);
#17142=PRODUCT_DEFINITION_FORMATION('',$,#17241);
#17207=APPLICATION_CONTEXT(
'Core Data for Automotive Mechanical Design Process');
#17208=PRODUCT_CONTEXT('part definition',#17207,'mechanical');
#17241=PRODUCT('Right screw nut','Right screw nut','Right screw nut',(#17208));
#17327=COLOUR_RGB('Black',0.12,0.14,0.17);
#17328=FILL_AREA_STYLE_COLOUR('',#17327);
#17329=FILL_AREA_STYLE('',(#17328));
#17330=SURFACE_STYLE_FILL_AREA(#17329);
#17331=SURFACE_SIDE_STYLE('',(#17330));
#17332=SURFACE_STYLE_USAGE(.BOTH.,#17331);
#17333=PRESENTATION_STYLE_ASSIGNMENT((#17332));
ENDSEC;
END-ISO-10303-21;
